ISO-10303-21;
HEADER;
/* Generated by software containing ST-Developer
 * from STEP Tools, Inc. (www.steptools.com) 
 */

FILE_DESCRIPTION(
/* description */ (''),
/* implementation_level */ '2;1');

FILE_NAME(
/* name */ 'Ball_Screw_03.step',
/* time_stamp */ '2026-10-23T17:00:58+06:00',
/* author */ (''),
/* organization */ (''),
/* preprocessor_version */ 'ST-DEVELOPER v20.2',
/* originating_system */ 'Autodesk Translation Framework v15.15.0.0',
/* authorisation */ '');

FILE_SCHEMA (('AUTOMOTIVE_DESIGN { 1 0 10303 214 3 1 1 }'));
ENDSEC;

DATA;
#10=MECHANICAL_DESIGN_GEOMETRIC_PRESENTATION_REPRESENTATION('',(#118),#11385);
#68=SPHERICAL_SURFACE('',#6077,3.);
#79=TOROIDAL_SURFACE('',#6080,2.65761552865316,0.5);
#92=SHAPE_REPRESENTATION_RELATIONSHIP('SRR','None',#11444,#105);
#105=ADVANCED_BREP_SHAPE_REPRESENTATION('',(#131),#11384);
#118=STYLED_ITEM('',(#11574),#131);
#131=MANIFOLD_SOLID_BREP('Ball_Screw_03',#5354);
#171=FACE_BOUND('',#1286,.T.);
#172=FACE_BOUND('',#1296,.T.);
#272=CONICAL_SURFACE('',#6094,2.90761552865316,0.785398163397448);
#528=CIRCLE('',#6078,2.59807621135332);
#529=CIRCLE('',#6079,3.);
#530=CIRCLE('',#6081,2.65761552865316);
#531=CIRCLE('',#6082,0.5);
#532=CIRCLE('',#6083,3.15761552865316);
#533=CIRCLE('',#6085,3.15761552865316);
#534=CIRCLE('',#6095,2.65761552865316);
#603=CYLINDRICAL_SURFACE('',#6084,3.15761552865316);
#917=FACE_OUTER_BOUND('',#1282,.T.);
#918=FACE_OUTER_BOUND('',#1283,.T.);
#919=FACE_OUTER_BOUND('',#1284,.T.);
#920=FACE_OUTER_BOUND('',#1285,.T.);
#921=FACE_OUTER_BOUND('',#1287,.T.);
#922=FACE_OUTER_BOUND('',#1288,.T.);
#923=FACE_OUTER_BOUND('',#1289,.T.);
#924=FACE_OUTER_BOUND('',#1290,.T.);
#925=FACE_OUTER_BOUND('',#1291,.T.);
#926=FACE_OUTER_BOUND('',#1292,.T.);
#927=FACE_OUTER_BOUND('',#1293,.T.);
#928=FACE_OUTER_BOUND('',#1294,.T.);
#929=FACE_OUTER_BOUND('',#1295,.T.);
#1282=EDGE_LOOP('',(#4812,#4813,#4814));
#1283=EDGE_LOOP('',(#4815,#4816,#4817,#4818));
#1284=EDGE_LOOP('',(#4819,#4820,#4821,#4822));
#1285=EDGE_LOOP('',(#4823));
#1286=EDGE_LOOP('',(#4824));
#1287=EDGE_LOOP('',(#4825,#4826,#4827,#4828));
#1288=EDGE_LOOP('',(#4829,#4830,#4831,#4832));
#1289=EDGE_LOOP('',(#4833,#4834,#4835,#4836));
#1290=EDGE_LOOP('',(#4837,#4838,#4839,#4840));
#1291=EDGE_LOOP('',(#4841,#4842,#4843,#4844));
#1292=EDGE_LOOP('',(#4845,#4846,#4847,#4848));
#1293=EDGE_LOOP('',(#4849,#4850,#4851,#4852,#4853,#4854));
#1294=EDGE_LOOP('',(#4855,#4856,#4857,#4858));
#1295=EDGE_LOOP('',(#4859));
#1296=EDGE_LOOP('',(#4860,#4861,#4862,#4863,#4864,#4865));
#1739=LINE('',#11298,#2201);
#1740=LINE('',#11304,#2202);
#1741=LINE('',#11306,#2203);
#1742=LINE('',#11308,#2204);
#1743=LINE('',#11309,#2205);
#1744=LINE('',#11312,#2206);
#1745=LINE('',#11314,#2207);
#1746=LINE('',#11315,#2208);
#1747=LINE('',#11318,#2209);
#1748=LINE('',#11320,#2210);
#1749=LINE('',#11321,#2211);
#1750=LINE('',#11324,#2212);
#1751=LINE('',#11326,#2213);
#1752=LINE('',#11327,#2214);
#1753=LINE('',#11330,#2215);
#1754=LINE('',#11332,#2216);
#1755=LINE('',#11333,#2217);
#1756=LINE('',#11335,#2218);
#1757=LINE('',#11336,#2219);
#1758=LINE('',#11341,#2220);
#2201=VECTOR('',#7724,3.15761552865316);
#2202=VECTOR('',#7731,10.);
#2203=VECTOR('',#7732,10.);
#2204=VECTOR('',#7733,10.);
#2205=VECTOR('',#7734,10.);
#2206=VECTOR('',#7737,10.);
#2207=VECTOR('',#7738,10.);
#2208=VECTOR('',#7739,10.);
#2209=VECTOR('',#7742,10.);
#2210=VECTOR('',#7743,10.);
#2211=VECTOR('',#7744,10.);
#2212=VECTOR('',#7747,10.);
#2213=VECTOR('',#7748,10.);
#2214=VECTOR('',#7749,10.);
#2215=VECTOR('',#7752,10.);
#2216=VECTOR('',#7753,10.);
#2217=VECTOR('',#7754,10.);
#2218=VECTOR('',#7757,10.);
#2219=VECTOR('',#7758,10.);
#2220=VECTOR('',#7765,2.90761552865316);
#2646=VERTEX_POINT('',#11286);
#2647=VERTEX_POINT('',#11288);
#2648=VERTEX_POINT('',#11291);
#2649=VERTEX_POINT('',#11293);
#2650=VERTEX_POINT('',#11297);
#2651=VERTEX_POINT('',#11302);
#2652=VERTEX_POINT('',#11303);
#2653=VERTEX_POINT('',#11305);
#2654=VERTEX_POINT('',#11307);
#2655=VERTEX_POINT('',#11311);
#2656=VERTEX_POINT('',#11313);
#2657=VERTEX_POINT('',#11317);
#2658=VERTEX_POINT('',#11319);
#2659=VERTEX_POINT('',#11323);
#2660=VERTEX_POINT('',#11325);
#2661=VERTEX_POINT('',#11329);
#2662=VERTEX_POINT('',#11331);
#2663=VERTEX_POINT('',#11339);
#3371=EDGE_CURVE('',#2646,#2646,#528,.T.);
#3372=EDGE_CURVE('',#2647,#2646,#529,.T.);
#3373=EDGE_CURVE('',#2648,#2648,#530,.T.);
#3374=EDGE_CURVE('',#2648,#2649,#531,.T.);
#3375=EDGE_CURVE('',#2649,#2649,#532,.T.);
#3376=EDGE_CURVE('',#2649,#2650,#1739,.T.);
#3377=EDGE_CURVE('',#2650,#2650,#533,.T.);
#3378=EDGE_CURVE('',#2651,#2652,#1740,.T.);
#3379=EDGE_CURVE('',#2651,#2653,#1741,.T.);
#3380=EDGE_CURVE('',#2653,#2654,#1742,.T.);
#3381=EDGE_CURVE('',#2652,#2654,#1743,.T.);
#3382=EDGE_CURVE('',#2655,#2651,#1744,.T.);
#3383=EDGE_CURVE('',#2655,#2656,#1745,.T.);
#3384=EDGE_CURVE('',#2656,#2653,#1746,.T.);
#3385=EDGE_CURVE('',#2657,#2655,#1747,.T.);
#3386=EDGE_CURVE('',#2657,#2658,#1748,.T.);
#3387=EDGE_CURVE('',#2658,#2656,#1749,.T.);
#3388=EDGE_CURVE('',#2659,#2657,#1750,.T.);
#3389=EDGE_CURVE('',#2659,#2660,#1751,.T.);
#3390=EDGE_CURVE('',#2660,#2658,#1752,.T.);
#3391=EDGE_CURVE('',#2661,#2659,#1753,.T.);
#3392=EDGE_CURVE('',#2661,#2662,#1754,.T.);
#3393=EDGE_CURVE('',#2662,#2660,#1755,.T.);
#3394=EDGE_CURVE('',#2652,#2661,#1756,.T.);
#3395=EDGE_CURVE('',#2654,#2662,#1757,.T.);
#3396=EDGE_CURVE('',#2663,#2663,#534,.T.);
#3397=EDGE_CURVE('',#2663,#2650,#1758,.T.);
#4812=ORIENTED_EDGE('',*,*,#3371,.F.);
#4813=ORIENTED_EDGE('',*,*,#3372,.F.);
#4814=ORIENTED_EDGE('',*,*,#3372,.T.);
#4815=ORIENTED_EDGE('',*,*,#3373,.T.);
#4816=ORIENTED_EDGE('',*,*,#3374,.T.);
#4817=ORIENTED_EDGE('',*,*,#3375,.T.);
#4818=ORIENTED_EDGE('',*,*,#3374,.F.);
#4819=ORIENTED_EDGE('',*,*,#3375,.F.);
#4820=ORIENTED_EDGE('',*,*,#3376,.T.);
#4821=ORIENTED_EDGE('',*,*,#3377,.F.);
#4822=ORIENTED_EDGE('',*,*,#3376,.F.);
#4823=ORIENTED_EDGE('',*,*,#3373,.F.);
#4824=ORIENTED_EDGE('',*,*,#3371,.T.);
#4825=ORIENTED_EDGE('',*,*,#3378,.F.);
#4826=ORIENTED_EDGE('',*,*,#3379,.T.);
#4827=ORIENTED_EDGE('',*,*,#3380,.T.);
#4828=ORIENTED_EDGE('',*,*,#3381,.F.);
#4829=ORIENTED_EDGE('',*,*,#3382,.F.);
#4830=ORIENTED_EDGE('',*,*,#3383,.T.);
#4831=ORIENTED_EDGE('',*,*,#3384,.T.);
#4832=ORIENTED_EDGE('',*,*,#3379,.F.);
#4833=ORIENTED_EDGE('',*,*,#3385,.F.);
#4834=ORIENTED_EDGE('',*,*,#3386,.T.);
#4835=ORIENTED_EDGE('',*,*,#3387,.T.);
#4836=ORIENTED_EDGE('',*,*,#3383,.F.);
#4837=ORIENTED_EDGE('',*,*,#3388,.F.);
#4838=ORIENTED_EDGE('',*,*,#3389,.T.);
#4839=ORIENTED_EDGE('',*,*,#3390,.T.);
#4840=ORIENTED_EDGE('',*,*,#3386,.F.);
#4841=ORIENTED_EDGE('',*,*,#3391,.F.);
#4842=ORIENTED_EDGE('',*,*,#3392,.T.);
#4843=ORIENTED_EDGE('',*,*,#3393,.T.);
#4844=ORIENTED_EDGE('',*,*,#3389,.F.);
#4845=ORIENTED_EDGE('',*,*,#3394,.F.);
#4846=ORIENTED_EDGE('',*,*,#3381,.T.);
#4847=ORIENTED_EDGE('',*,*,#3395,.T.);
#4848=ORIENTED_EDGE('',*,*,#3392,.F.);
#4849=ORIENTED_EDGE('',*,*,#3395,.F.);
#4850=ORIENTED_EDGE('',*,*,#3380,.F.);
#4851=ORIENTED_EDGE('',*,*,#3384,.F.);
#4852=ORIENTED_EDGE('',*,*,#3387,.F.);
#4853=ORIENTED_EDGE('',*,*,#3390,.F.);
#4854=ORIENTED_EDGE('',*,*,#3393,.F.);
#4855=ORIENTED_EDGE('',*,*,#3396,.T.);
#4856=ORIENTED_EDGE('',*,*,#3397,.T.);
#4857=ORIENTED_EDGE('',*,*,#3377,.T.);
#4858=ORIENTED_EDGE('',*,*,#3397,.F.);
#4859=ORIENTED_EDGE('',*,*,#3396,.F.);
#4860=ORIENTED_EDGE('',*,*,#3378,.T.);
#4861=ORIENTED_EDGE('',*,*,#3394,.T.);
#4862=ORIENTED_EDGE('',*,*,#3391,.T.);
#4863=ORIENTED_EDGE('',*,*,#3388,.T.);
#4864=ORIENTED_EDGE('',*,*,#3385,.T.);
#4865=ORIENTED_EDGE('',*,*,#3382,.T.);
#5007=PLANE('',#6086);
#5008=PLANE('',#6087);
#5009=PLANE('',#6088);
#5010=PLANE('',#6089);
#5011=PLANE('',#6090);
#5012=PLANE('',#6091);
#5013=PLANE('',#6092);
#5014=PLANE('',#6093);
#5015=PLANE('',#6096);
#5329=ADVANCED_FACE('',(#917),#68,.T.);
#5330=ADVANCED_FACE('',(#918),#79,.T.);
#5331=ADVANCED_FACE('',(#919),#603,.T.);
#5332=ADVANCED_FACE('',(#920,#171),#5007,.F.);
#5333=ADVANCED_FACE('',(#921),#5008,.F.);
#5334=ADVANCED_FACE('',(#922),#5009,.F.);
#5335=ADVANCED_FACE('',(#923),#5010,.F.);
#5336=ADVANCED_FACE('',(#924),#5011,.F.);
#5337=ADVANCED_FACE('',(#925),#5012,.F.);
#5338=ADVANCED_FACE('',(#926),#5013,.F.);
#5339=ADVANCED_FACE('',(#927),#5014,.F.);
#5340=ADVANCED_FACE('',(#928),#272,.T.);
#5341=ADVANCED_FACE('',(#929,#172),#5015,.T.);
#5354=CLOSED_SHELL('',(#5329,#5330,#5331,#5332,#5333,#5334,#5335,#5336,
#5337,#5338,#5339,#5340,#5341));
#6076=AXIS2_PLACEMENT_3D('',#11284,#7706,#7707);
#6077=AXIS2_PLACEMENT_3D('',#11285,#7708,#7709);
#6078=AXIS2_PLACEMENT_3D('',#11287,#7710,#7711);
#6079=AXIS2_PLACEMENT_3D('',#11289,#7712,#7713);
#6080=AXIS2_PLACEMENT_3D('',#11290,#7714,#7715);
#6081=AXIS2_PLACEMENT_3D('',#11292,#7716,#7717);
#6082=AXIS2_PLACEMENT_3D('',#11294,#7718,#7719);
#6083=AXIS2_PLACEMENT_3D('',#11295,#7720,#7721);
#6084=AXIS2_PLACEMENT_3D('',#11296,#7722,#7723);
#6085=AXIS2_PLACEMENT_3D('',#11299,#7725,#7726);
#6086=AXIS2_PLACEMENT_3D('',#11300,#7727,#7728);
#6087=AXIS2_PLACEMENT_3D('',#11301,#7729,#7730);
#6088=AXIS2_PLACEMENT_3D('',#11310,#7735,#7736);
#6089=AXIS2_PLACEMENT_3D('',#11316,#7740,#7741);
#6090=AXIS2_PLACEMENT_3D('',#11322,#7745,#7746);
#6091=AXIS2_PLACEMENT_3D('',#11328,#7750,#7751);
#6092=AXIS2_PLACEMENT_3D('',#11334,#7755,#7756);
#6093=AXIS2_PLACEMENT_3D('',#11337,#7759,#7760);
#6094=AXIS2_PLACEMENT_3D('',#11338,#7761,#7762);
#6095=AXIS2_PLACEMENT_3D('',#11340,#7763,#7764);
#6096=AXIS2_PLACEMENT_3D('',#11342,#7766,#7767);
#7706=DIRECTION('axis',(0.,0.,1.));
#7707=DIRECTION('refdir',(1.,0.,0.));
#7708=DIRECTION('center_axis',(0.,0.,-1.));
#7709=DIRECTION('ref_axis',(1.,0.,0.));
#7710=DIRECTION('center_axis',(0.,-1.22464679914735E-16,1.));
#7711=DIRECTION('ref_axis',(0.,-1.,-1.22464679914735E-16));
#7712=DIRECTION('center_axis',(0.,1.,1.22464679914735E-16));
#7713=DIRECTION('ref_axis',(-1.,0.,0.));
#7714=DIRECTION('center_axis',(0.,1.22464679914735E-16,-1.));
#7715=DIRECTION('ref_axis',(1.,0.,0.));
#7716=DIRECTION('center_axis',(0.,-1.22464679914735E-16,1.));
#7717=DIRECTION('ref_axis',(1.,0.,0.));
#7718=DIRECTION('center_axis',(0.,1.,1.22464679914735E-16));
#7719=DIRECTION('ref_axis',(-1.,0.,0.));
#7720=DIRECTION('center_axis',(0.,1.22464679914735E-16,-1.));
#7721=DIRECTION('ref_axis',(1.,0.,0.));
#7722=DIRECTION('center_axis',(0.,1.22464679914735E-16,-1.));
#7723=DIRECTION('ref_axis',(1.,0.,0.));
#7724=DIRECTION('',(0.,-1.22464679914735E-16,1.));
#7725=DIRECTION('center_axis',(0.,-1.22464679914735E-16,1.));
#7726=DIRECTION('ref_axis',(1.,0.,0.));
#7727=DIRECTION('center_axis',(0.,-1.22464679914735E-16,1.));
#7728=DIRECTION('ref_axis',(1.,0.,0.));
#7729=DIRECTION('center_axis',(-0.5,-0.866025403784439,-1.06057523872491E-16));
#7730=DIRECTION('ref_axis',(-0.866025403784439,0.5,6.12323399573677E-17));
#7731=DIRECTION('',(-0.866025403784439,0.5,6.12323399573677E-17));
#7732=DIRECTION('',(0.,1.22464679914735E-16,-1.));
#7733=DIRECTION('',(-0.866025403784439,0.5,6.12323399573677E-17));
#7734=DIRECTION('',(0.,1.22464679914735E-16,-1.));
#7735=DIRECTION('center_axis',(0.5,-0.866025403784439,-1.06057523872491E-16));
#7736=DIRECTION('ref_axis',(-0.866025403784439,-0.5,-6.12323399573677E-17));
#7737=DIRECTION('',(-0.866025403784439,-0.5,-6.12323399573677E-17));
#7738=DIRECTION('',(0.,1.22464679914735E-16,-1.));
#7739=DIRECTION('',(-0.866025403784439,-0.5,-6.12323399573677E-17));
#7740=DIRECTION('center_axis',(1.,0.,0.));
#7741=DIRECTION('ref_axis',(0.,-1.,-1.22464679914735E-16));
#7742=DIRECTION('',(0.,-1.,-1.22464679914735E-16));
#7743=DIRECTION('',(0.,1.22464679914735E-16,-1.));
#7744=DIRECTION('',(0.,-1.,-1.22464679914735E-16));
#7745=DIRECTION('center_axis',(0.5,0.866025403784439,1.06057523872491E-16));
#7746=DIRECTION('ref_axis',(0.866025403784439,-0.5,-6.12323399573677E-17));
#7747=DIRECTION('',(0.866025403784439,-0.5,-6.12323399573677E-17));
#7748=DIRECTION('',(0.,1.22464679914735E-16,-1.));
#7749=DIRECTION('',(0.866025403784439,-0.5,-6.12323399573677E-17));
#7750=DIRECTION('center_axis',(-0.5,0.866025403784439,1.06057523872491E-16));
#7751=DIRECTION('ref_axis',(0.866025403784439,0.5,6.12323399573676E-17));
#7752=DIRECTION('',(0.866025403784439,0.5,6.12323399573676E-17));
#7753=DIRECTION('',(0.,1.22464679914735E-16,-1.));
#7754=DIRECTION('',(0.866025403784439,0.5,6.12323399573676E-17));
#7755=DIRECTION('center_axis',(-1.,6.40987562127855E-16,7.84983366253143E-32));
#7756=DIRECTION('ref_axis',(6.40987562127855E-16,1.,1.22464679914735E-16));
#7757=DIRECTION('',(6.40987562127855E-16,1.,1.22464679914735E-16));
#7758=DIRECTION('',(6.40987562127855E-16,1.,1.22464679914735E-16));
#7759=DIRECTION('center_axis',(0.,1.22464679914735E-16,-1.));
#7760=DIRECTION('ref_axis',(1.,0.,0.));
#7761=DIRECTION('center_axis',(0.,1.22464679914735E-16,-1.));
#7762=DIRECTION('ref_axis',(1.,0.,0.));
#7763=DIRECTION('center_axis',(0.,1.22464679914735E-16,-1.));
#7764=DIRECTION('ref_axis',(1.,0.,0.));
#7765=DIRECTION('',(-0.707106781186547,2.11959791839945E-32,-0.707106781186548));
#7766=DIRECTION('center_axis',(0.,-1.22464679914735E-16,1.));
#7767=DIRECTION('ref_axis',(1.,0.,0.));
#11284=CARTESIAN_POINT('',(0.,0.,0.));
#11285=CARTESIAN_POINT('Origin',(-24.6892783072069,25.1107216927931,9.2));
#11286=CARTESIAN_POINT('',(-27.2873545185602,25.1107216927931,7.7));
#11287=CARTESIAN_POINT('Origin',(-24.6892783072069,25.1107216927931,7.7));
#11288=CARTESIAN_POINT('',(-24.6892783072069,25.1107216927931,6.2));
#11289=CARTESIAN_POINT('Origin',(-24.6892783072069,25.1107216927931,9.2));
#11290=CARTESIAN_POINT('Origin',(-24.6892783072069,25.1107216927931,8.2));
#11291=CARTESIAN_POINT('',(-27.3468938358601,25.1107216927931,7.7));
#11292=CARTESIAN_POINT('Origin',(-24.6892783072069,25.1107216927931,7.7));
#11293=CARTESIAN_POINT('',(-27.8468938358601,25.1107216927931,8.2));
#11294=CARTESIAN_POINT('Origin',(-27.3468938358601,25.1107216927931,8.2));
#11295=CARTESIAN_POINT('Origin',(-24.6892783072069,25.1107216927931,8.2));
#11296=CARTESIAN_POINT('Origin',(-24.6892783072069,25.1107216927931,19.));
#11297=CARTESIAN_POINT('',(-27.8468938358601,25.1107216927931,18.5));
#11298=CARTESIAN_POINT('',(-27.8468938358601,25.1107216927931,19.));
#11299=CARTESIAN_POINT('Origin',(-24.6892783072069,25.1107216927931,18.5));
#11300=CARTESIAN_POINT('Origin',(-24.6892783072069,25.1107216927931,7.7));
#11301=CARTESIAN_POINT('Origin',(-24.6892783072069,23.3786708852242,19.));
#11302=CARTESIAN_POINT('',(-24.6892783072069,23.3786708852242,19.));
#11303=CARTESIAN_POINT('',(-26.1892783072069,24.2446962890086,19.));
#11304=CARTESIAN_POINT('',(-25.0642783072069,23.5951772361703,19.));
#11305=CARTESIAN_POINT('',(-24.6892783072069,23.3786708852242,18.));
#11306=CARTESIAN_POINT('',(-24.6892783072069,23.3786708852242,19.));
#11307=CARTESIAN_POINT('',(-26.1892783072069,24.2446962890086,18.));
#11308=CARTESIAN_POINT('',(-26.1892783072069,24.2446962890086,18.));
#11309=CARTESIAN_POINT('',(-26.1892783072069,24.2446962890086,19.));
#11310=CARTESIAN_POINT('Origin',(-23.1892783072069,24.2446962890086,19.));
#11311=CARTESIAN_POINT('',(-23.1892783072069,24.2446962890086,19.));
#11312=CARTESIAN_POINT('',(-23.5642783072069,24.0281899380625,19.));
#11313=CARTESIAN_POINT('',(-23.1892783072069,24.2446962890086,18.));
#11314=CARTESIAN_POINT('',(-23.1892783072069,24.2446962890086,19.));
#11315=CARTESIAN_POINT('',(-24.6892783072069,23.3786708852242,18.));
#11316=CARTESIAN_POINT('Origin',(-23.1892783072069,25.9767470965775,19.));
#11317=CARTESIAN_POINT('',(-23.1892783072069,25.9767470965775,19.));
#11318=CARTESIAN_POINT('',(-23.1892783072069,25.5437343946853,19.));
#11319=CARTESIAN_POINT('',(-23.1892783072069,25.9767470965775,18.));
#11320=CARTESIAN_POINT('',(-23.1892783072069,25.9767470965775,19.));
#11321=CARTESIAN_POINT('',(-23.1892783072069,24.2446962890086,18.));
#11322=CARTESIAN_POINT('Origin',(-24.6892783072069,26.842772500362,19.));
#11323=CARTESIAN_POINT('',(-24.6892783072069,26.842772500362,19.));
#11324=CARTESIAN_POINT('',(-24.3142783072069,26.6262661494158,19.));
#11325=CARTESIAN_POINT('',(-24.6892783072069,26.842772500362,18.));
#11326=CARTESIAN_POINT('',(-24.6892783072069,26.842772500362,19.));
#11327=CARTESIAN_POINT('',(-23.1892783072069,25.9767470965775,18.));
#11328=CARTESIAN_POINT('Origin',(-26.1892783072069,25.9767470965775,19.));
#11329=CARTESIAN_POINT('',(-26.1892783072069,25.9767470965775,19.));
#11330=CARTESIAN_POINT('',(-25.8142783072069,26.1932534475236,19.));
#11331=CARTESIAN_POINT('',(-26.1892783072069,25.9767470965775,18.));
#11332=CARTESIAN_POINT('',(-26.1892783072069,25.9767470965775,19.));
#11333=CARTESIAN_POINT('',(-24.6892783072069,26.842772500362,18.));
#11334=CARTESIAN_POINT('Origin',(-26.1892783072069,24.2446962890086,19.));
#11335=CARTESIAN_POINT('',(-26.1892783072069,24.6777089909009,19.));
#11336=CARTESIAN_POINT('',(-26.1892783072069,25.9767470965775,18.));
#11337=CARTESIAN_POINT('Origin',(-24.6892783072069,25.1107216927931,18.));
#11338=CARTESIAN_POINT('Origin',(-24.6892783072069,25.1107216927931,18.75));
#11339=CARTESIAN_POINT('',(-27.3468938358601,25.1107216927931,19.));
#11340=CARTESIAN_POINT('Origin',(-24.6892783072069,25.1107216927931,19.));
#11341=CARTESIAN_POINT('',(-27.5968938358601,25.1107216927931,18.75));
#11342=CARTESIAN_POINT('Origin',(-24.6892783072069,25.1107216927931,19.));
#11369=UNCERTAINTY_MEASURE_WITH_UNIT(LENGTH_MEASURE(0.01),#11386,
'DISTANCE_ACCURACY_VALUE',
'Maximum model space distance between geometric entities at asserted c
onnectivities');
#11370=UNCERTAINTY_MEASURE_WITH_UNIT(LENGTH_MEASURE(0.01),#11386,
'DISTANCE_ACCURACY_VALUE',
'Maximum model space distance between geometric entities at asserted c
onnectivities');
#11384=(
GEOMETRIC_REPRESENTATION_CONTEXT(3)
GLOBAL_UNCERTAINTY_ASSIGNED_CONTEXT((#11369))
GLOBAL_UNIT_ASSIGNED_CONTEXT((#11386,#11388,#11389))
REPRESENTATION_CONTEXT('','3D')
);
#11385=(
GEOMETRIC_REPRESENTATION_CONTEXT(3)
GLOBAL_UNCERTAINTY_ASSIGNED_CONTEXT((#11370))
GLOBAL_UNIT_ASSIGNED_CONTEXT((#11386,#11388,#11389))
REPRESENTATION_CONTEXT('','3D')
);
#11386=(
LENGTH_UNIT()
NAMED_UNIT(*)
SI_UNIT(.MILLI.,.METRE.)
);
#11388=(
NAMED_UNIT(*)
PLANE_ANGLE_UNIT()
SI_UNIT($,.RADIAN.)
);
#11389=(
NAMED_UNIT(*)
SI_UNIT($,.STERADIAN.)
SOLID_ANGLE_UNIT()
);
#11403=SHAPE_DEFINITION_REPRESENTATION(#11417,#11444);
#11417=PRODUCT_DEFINITION_SHAPE('',$,#11459);
#11444=SHAPE_REPRESENTATION('',(#6076),#11384);
#11445=PRODUCT_DEFINITION_CONTEXT('part definition',#11489,'design');
#11459=PRODUCT_DEFINITION('Ball_Screw_03','Ball_Screw_03',#11473,#11445);
#11473=PRODUCT_DEFINITION_FORMATION('',$,#11504);
#11489=APPLICATION_CONTEXT(
'Core Data for Automotive Mechanical Design Process');
#11490=PRODUCT_CONTEXT('part definition',#11489,'mechanical');
#11504=PRODUCT('Ball_Screw_03','Ball_Screw_03',$,(#11490));
#11568=COLOUR_RGB('Black',0.12,0.14,0.17);
#11569=FILL_AREA_STYLE_COLOUR('',#11568);
#11570=FILL_AREA_STYLE('',(#11569));
#11571=SURFACE_STYLE_FILL_AREA(#11570);
#11572=SURFACE_SIDE_STYLE('',(#11571));
#11573=SURFACE_STYLE_USAGE(.BOTH.,#11572);
#11574=PRESENTATION_STYLE_ASSIGNMENT((#11573));
ENDSEC;
END-ISO-10303-21;
